ISO-10303-21;
HEADER;
/* Generated by software containing ST-Developer
 * from STEP Tools, Inc. (www.steptools.com) 
 */

FILE_DESCRIPTION(
/* description */ ('Rack and pinion manual slide'),
/* implementation_level */ '2;1');

FILE_NAME(
/* name */ 'Cap Screw - M5x20.step',
/* time_stamp */ '2026-10-28T03:22:49-07:00',
/* author */ (''),
/* organization */ (''),
/* preprocessor_version */ 'ST-DEVELOPER v20.2',
/* originating_system */ 'Autodesk Translation Framework v15.17.0.0',
/* authorisation */ '');

FILE_SCHEMA (('AUTOMOTIVE_DESIGN { 1 0 10303 214 3 1 1 }'));
ENDSEC;

DATA;
#10=MECHANICAL_DESIGN_GEOMETRIC_PRESENTATION_REPRESENTATION('',(#750),#34851);
#605=ORIENTED_CLOSED_SHELL('',*,#13771,.F.);
#610=BREP_WITH_VOIDS('Body1',#13770,(#605));
#616=CONICAL_SURFACE('',#14755,0.4,0.785398163397448);
#617=CONICAL_SURFACE('',#14759,0.41,0.785398163397448);
#618=CONICAL_SURFACE('',#14763,0.26,0.463647609000806);
#619=CONICAL_SURFACE('',#14767,0.225,0.785398163397448);
#658=SHAPE_REPRESENTATION_RELATIONSHIP('SRR','None',#35093,#704);
#704=ADVANCED_BREP_SHAPE_REPRESENTATION('',(#610),#34818);
#750=STYLED_ITEM('',(#35418),#610);
#974=FACE_BOUND('',#2666,.T.);
#1207=PLANE('',#14753);
#1208=PLANE('',#14761);
#1209=PLANE('',#14769);
#1210=PLANE('',#14770);
#1211=PLANE('',#14771);
#1212=PLANE('',#14772);
#1213=PLANE('',#14773);
#1214=PLANE('',#14774);
#1215=PLANE('',#14775);
#1216=PLANE('',#14776);
#1217=PLANE('',#14777);
#1781=FACE_OUTER_BOUND('',#2661,.T.);
#1782=FACE_OUTER_BOUND('',#2662,.T.);
#1783=FACE_OUTER_BOUND('',#2663,.T.);
#1784=FACE_OUTER_BOUND('',#2664,.T.);
#1785=FACE_OUTER_BOUND('',#2665,.T.);
#1786=FACE_OUTER_BOUND('',#2667,.T.);
#1787=FACE_OUTER_BOUND('',#2668,.T.);
#1788=FACE_OUTER_BOUND('',#2669,.T.);
#1789=FACE_OUTER_BOUND('',#2670,.T.);
#1790=FACE_OUTER_BOUND('',#2671,.T.);
#1791=FACE_OUTER_BOUND('',#2672,.T.);
#1792=FACE_OUTER_BOUND('',#2673,.T.);
#1793=FACE_OUTER_BOUND('',#2674,.T.);
#1794=FACE_OUTER_BOUND('',#2675,.T.);
#1795=FACE_OUTER_BOUND('',#2676,.T.);
#1796=FACE_OUTER_BOUND('',#2677,.T.);
#1797=FACE_OUTER_BOUND('',#2678,.T.);
#2661=EDGE_LOOP('',(#10426));
#2662=EDGE_LOOP('',(#10427,#10428,#10429,#10430));
#2663=EDGE_LOOP('',(#10431,#10432,#10433,#10434));
#2664=EDGE_LOOP('',(#10435,#10436,#10437,#10438));
#2665=EDGE_LOOP('',(#10439));
#2666=EDGE_LOOP('',(#10440));
#2667=EDGE_LOOP('',(#10441,#10442,#10443,#10444));
#2668=EDGE_LOOP('',(#10445,#10446,#10447,#10448));
#2669=EDGE_LOOP('',(#10449,#10450,#10451,#10452));
#2670=EDGE_LOOP('',(#10453));
#2671=EDGE_LOOP('',(#10454,#10455,#10456,#10457));
#2672=EDGE_LOOP('',(#10458,#10459,#10460,#10461));
#2673=EDGE_LOOP('',(#10462,#10463,#10464,#10465));
#2674=EDGE_LOOP('',(#10466,#10467,#10468,#10469));
#2675=EDGE_LOOP('',(#10470,#10471,#10472,#10473));
#2676=EDGE_LOOP('',(#10474,#10475,#10476,#10477));
#2677=EDGE_LOOP('',(#10478,#10479,#10480,#10481,#10482,#10483));
#2678=EDGE_LOOP('',(#10484,#10485,#10486,#10487,#10488,#10489));
#3651=LINE('',#20723,#4942);
#3652=LINE('',#20727,#4943);
#3653=LINE('',#20731,#4944);
#3654=LINE('',#20738,#4945);
#3655=LINE('',#20742,#4946);
#3656=LINE('',#20746,#4947);
#3657=LINE('',#20751,#4948);
#3658=LINE('',#20753,#4949);
#3659=LINE('',#20755,#4950);
#3660=LINE('',#20756,#4951);
#3661=LINE('',#20759,#4952);
#3662=LINE('',#20761,#4953);
#3663=LINE('',#20762,#4954);
#3664=LINE('',#20765,#4955);
#3665=LINE('',#20767,#4956);
#3666=LINE('',#20768,#4957);
#3667=LINE('',#20771,#4958);
#3668=LINE('',#20773,#4959);
#3669=LINE('',#20774,#4960);
#3670=LINE('',#20777,#4961);
#3671=LINE('',#20779,#4962);
#3672=LINE('',#20780,#4963);
#3673=LINE('',#20782,#4964);
#3674=LINE('',#20783,#4965);
#4942=VECTOR('',#16907,0.4);
#4943=VECTOR('',#16912,0.425);
#4944=VECTOR('',#16917,0.41);
#4945=VECTOR('',#16926,0.26);
#4946=VECTOR('',#16931,0.25);
#4947=VECTOR('',#16936,0.225);
#4948=VECTOR('',#16941,1.);
#4949=VECTOR('',#16942,1.);
#4950=VECTOR('',#16943,1.);
#4951=VECTOR('',#16944,1.);
#4952=VECTOR('',#16947,1.);
#4953=VECTOR('',#16948,1.);
#4954=VECTOR('',#16949,1.);
#4955=VECTOR('',#16952,1.);
#4956=VECTOR('',#16953,1.);
#4957=VECTOR('',#16954,1.);
#4958=VECTOR('',#16957,1.);
#4959=VECTOR('',#16958,1.);
#4960=VECTOR('',#16959,1.);
#4961=VECTOR('',#16962,1.);
#4962=VECTOR('',#16963,1.);
#4963=VECTOR('',#16964,1.);
#4964=VECTOR('',#16967,1.);
#4965=VECTOR('',#16968,1.);
#5973=CIRCLE('',#14754,0.375);
#5974=CIRCLE('',#14756,0.425);
#5975=CIRCLE('',#14758,0.425);
#5976=CIRCLE('',#14760,0.395);
#5977=CIRCLE('',#14762,0.27);
#5978=CIRCLE('',#14764,0.24505);
#5979=CIRCLE('',#14766,0.24505);
#5980=CIRCLE('',#14768,0.2);
#6621=VERTEX_POINT('',#20718);
#6622=VERTEX_POINT('',#20721);
#6623=VERTEX_POINT('',#20725);
#6624=VERTEX_POINT('',#20729);
#6625=VERTEX_POINT('',#20733);
#6626=VERTEX_POINT('',#20736);
#6627=VERTEX_POINT('',#20740);
#6628=VERTEX_POINT('',#20744);
#6629=VERTEX_POINT('',#20749);
#6630=VERTEX_POINT('',#20750);
#6631=VERTEX_POINT('',#20752);
#6632=VERTEX_POINT('',#20754);
#6633=VERTEX_POINT('',#20758);
#6634=VERTEX_POINT('',#20760);
#6635=VERTEX_POINT('',#20764);
#6636=VERTEX_POINT('',#20766);
#6637=VERTEX_POINT('',#20770);
#6638=VERTEX_POINT('',#20772);
#6639=VERTEX_POINT('',#20776);
#6640=VERTEX_POINT('',#20778);
#8025=EDGE_CURVE('',#6621,#6621,#5973,.T.);
#8026=EDGE_CURVE('',#6622,#6622,#5974,.T.);
#8027=EDGE_CURVE('',#6622,#6621,#3651,.T.);
#8028=EDGE_CURVE('',#6623,#6623,#5975,.T.);
#8029=EDGE_CURVE('',#6623,#6622,#3652,.T.);
#8030=EDGE_CURVE('',#6624,#6624,#5976,.T.);
#8031=EDGE_CURVE('',#6624,#6623,#3653,.T.);
#8032=EDGE_CURVE('',#6625,#6625,#5977,.T.);
#8033=EDGE_CURVE('',#6626,#6626,#5978,.F.);
#8034=EDGE_CURVE('',#6626,#6625,#3654,.T.);
#8035=EDGE_CURVE('',#6627,#6627,#5979,.F.);
#8036=EDGE_CURVE('',#6627,#6626,#3655,.T.);
#8037=EDGE_CURVE('',#6628,#6628,#5980,.T.);
#8038=EDGE_CURVE('',#6628,#6627,#3656,.T.);
#8039=EDGE_CURVE('',#6629,#6630,#3657,.T.);
#8040=EDGE_CURVE('',#6630,#6631,#3658,.T.);
#8041=EDGE_CURVE('',#6631,#6632,#3659,.T.);
#8042=EDGE_CURVE('',#6629,#6632,#3660,.T.);
#8043=EDGE_CURVE('',#6630,#6633,#3661,.T.);
#8044=EDGE_CURVE('',#6633,#6634,#3662,.T.);
#8045=EDGE_CURVE('',#6634,#6631,#3663,.T.);
#8046=EDGE_CURVE('',#6633,#6635,#3664,.T.);
#8047=EDGE_CURVE('',#6635,#6636,#3665,.T.);
#8048=EDGE_CURVE('',#6636,#6634,#3666,.T.);
#8049=EDGE_CURVE('',#6635,#6637,#3667,.T.);
#8050=EDGE_CURVE('',#6637,#6638,#3668,.T.);
#8051=EDGE_CURVE('',#6638,#6636,#3669,.T.);
#8052=EDGE_CURVE('',#6637,#6639,#3670,.T.);
#8053=EDGE_CURVE('',#6639,#6640,#3671,.T.);
#8054=EDGE_CURVE('',#6640,#6638,#3672,.T.);
#8055=EDGE_CURVE('',#6639,#6629,#3673,.T.);
#8056=EDGE_CURVE('',#6632,#6640,#3674,.T.);
#10426=ORIENTED_EDGE('',*,*,#8025,.F.);
#10427=ORIENTED_EDGE('',*,*,#8026,.F.);
#10428=ORIENTED_EDGE('',*,*,#8027,.T.);
#10429=ORIENTED_EDGE('',*,*,#8025,.T.);
#10430=ORIENTED_EDGE('',*,*,#8027,.F.);
#10431=ORIENTED_EDGE('',*,*,#8028,.F.);
#10432=ORIENTED_EDGE('',*,*,#8029,.T.);
#10433=ORIENTED_EDGE('',*,*,#8026,.T.);
#10434=ORIENTED_EDGE('',*,*,#8029,.F.);
#10435=ORIENTED_EDGE('',*,*,#8030,.F.);
#10436=ORIENTED_EDGE('',*,*,#8031,.T.);
#10437=ORIENTED_EDGE('',*,*,#8028,.T.);
#10438=ORIENTED_EDGE('',*,*,#8031,.F.);
#10439=ORIENTED_EDGE('',*,*,#8030,.T.);
#10440=ORIENTED_EDGE('',*,*,#8032,.F.);
#10441=ORIENTED_EDGE('',*,*,#8033,.F.);
#10442=ORIENTED_EDGE('',*,*,#8034,.T.);
#10443=ORIENTED_EDGE('',*,*,#8032,.T.);
#10444=ORIENTED_EDGE('',*,*,#8034,.F.);
#10445=ORIENTED_EDGE('',*,*,#8035,.F.);
#10446=ORIENTED_EDGE('',*,*,#8036,.T.);
#10447=ORIENTED_EDGE('',*,*,#8033,.T.);
#10448=ORIENTED_EDGE('',*,*,#8036,.F.);
#10449=ORIENTED_EDGE('',*,*,#8037,.F.);
#10450=ORIENTED_EDGE('',*,*,#8038,.T.);
#10451=ORIENTED_EDGE('',*,*,#8035,.T.);
#10452=ORIENTED_EDGE('',*,*,#8038,.F.);
#10453=ORIENTED_EDGE('',*,*,#8037,.T.);
#10454=ORIENTED_EDGE('',*,*,#8039,.T.);
#10455=ORIENTED_EDGE('',*,*,#8040,.T.);
#10456=ORIENTED_EDGE('',*,*,#8041,.T.);
#10457=ORIENTED_EDGE('',*,*,#8042,.F.);
#10458=ORIENTED_EDGE('',*,*,#8043,.T.);
#10459=ORIENTED_EDGE('',*,*,#8044,.T.);
#10460=ORIENTED_EDGE('',*,*,#8045,.T.);
#10461=ORIENTED_EDGE('',*,*,#8040,.F.);
#10462=ORIENTED_EDGE('',*,*,#8046,.T.);
#10463=ORIENTED_EDGE('',*,*,#8047,.T.);
#10464=ORIENTED_EDGE('',*,*,#8048,.T.);
#10465=ORIENTED_EDGE('',*,*,#8044,.F.);
#10466=ORIENTED_EDGE('',*,*,#8049,.T.);
#10467=ORIENTED_EDGE('',*,*,#8050,.T.);
#10468=ORIENTED_EDGE('',*,*,#8051,.T.);
#10469=ORIENTED_EDGE('',*,*,#8047,.F.);
#10470=ORIENTED_EDGE('',*,*,#8052,.T.);
#10471=ORIENTED_EDGE('',*,*,#8053,.T.);
#10472=ORIENTED_EDGE('',*,*,#8054,.T.);
#10473=ORIENTED_EDGE('',*,*,#8050,.F.);
#10474=ORIENTED_EDGE('',*,*,#8055,.T.);
#10475=ORIENTED_EDGE('',*,*,#8042,.T.);
#10476=ORIENTED_EDGE('',*,*,#8056,.T.);
#10477=ORIENTED_EDGE('',*,*,#8053,.F.);
#10478=ORIENTED_EDGE('',*,*,#8055,.F.);
#10479=ORIENTED_EDGE('',*,*,#8052,.F.);
#10480=ORIENTED_EDGE('',*,*,#8049,.F.);
#10481=ORIENTED_EDGE('',*,*,#8046,.F.);
#10482=ORIENTED_EDGE('',*,*,#8043,.F.);
#10483=ORIENTED_EDGE('',*,*,#8039,.F.);
#10484=ORIENTED_EDGE('',*,*,#8056,.F.);
#10485=ORIENTED_EDGE('',*,*,#8041,.F.);
#10486=ORIENTED_EDGE('',*,*,#8045,.F.);
#10487=ORIENTED_EDGE('',*,*,#8048,.F.);
#10488=ORIENTED_EDGE('',*,*,#8051,.F.);
#10489=ORIENTED_EDGE('',*,*,#8054,.F.);
#12926=CYLINDRICAL_SURFACE('',#14757,0.425);
#12927=CYLINDRICAL_SURFACE('',#14765,0.24505);
#13259=ADVANCED_FACE('',(#1781),#1207,.T.);
#13260=ADVANCED_FACE('',(#1782),#616,.T.);
#13261=ADVANCED_FACE('',(#1783),#12926,.T.);
#13262=ADVANCED_FACE('',(#1784),#617,.T.);
#13263=ADVANCED_FACE('',(#1785,#974),#1208,.T.);
#13264=ADVANCED_FACE('',(#1786),#618,.T.);
#13265=ADVANCED_FACE('',(#1787),#12927,.T.);
#13266=ADVANCED_FACE('',(#1788),#619,.T.);
#13267=ADVANCED_FACE('',(#1789),#1209,.T.);
#13268=ADVANCED_FACE('',(#1790),#1210,.F.);
#13269=ADVANCED_FACE('',(#1791),#1211,.F.);
#13270=ADVANCED_FACE('',(#1792),#1212,.F.);
#13271=ADVANCED_FACE('',(#1793),#1213,.F.);
#13272=ADVANCED_FACE('',(#1794),#1214,.F.);
#13273=ADVANCED_FACE('',(#1795),#1215,.F.);
#13274=ADVANCED_FACE('',(#1796),#1216,.F.);
#13275=ADVANCED_FACE('',(#1797),#1217,.F.);
#13770=CLOSED_SHELL('',(#13259,#13260,#13261,#13262,#13263,#13264,#13265,
#13266,#13267));
#13771=CLOSED_SHELL('',(#13268,#13269,#13270,#13271,#13272,#13273,#13274,
#13275));
#14752=AXIS2_PLACEMENT_3D('',#20716,#16897,#16898);
#14753=AXIS2_PLACEMENT_3D('',#20717,#16899,#16900);
#14754=AXIS2_PLACEMENT_3D('',#20719,#16901,#16902);
#14755=AXIS2_PLACEMENT_3D('',#20720,#16903,#16904);
#14756=AXIS2_PLACEMENT_3D('',#20722,#16905,#16906);
#14757=AXIS2_PLACEMENT_3D('',#20724,#16908,#16909);
#14758=AXIS2_PLACEMENT_3D('',#20726,#16910,#16911);
#14759=AXIS2_PLACEMENT_3D('',#20728,#16913,#16914);
#14760=AXIS2_PLACEMENT_3D('',#20730,#16915,#16916);
#14761=AXIS2_PLACEMENT_3D('',#20732,#16918,#16919);
#14762=AXIS2_PLACEMENT_3D('',#20734,#16920,#16921);
#14763=AXIS2_PLACEMENT_3D('',#20735,#16922,#16923);
#14764=AXIS2_PLACEMENT_3D('',#20737,#16924,#16925);
#14765=AXIS2_PLACEMENT_3D('',#20739,#16927,#16928);
#14766=AXIS2_PLACEMENT_3D('',#20741,#16929,#16930);
#14767=AXIS2_PLACEMENT_3D('',#20743,#16932,#16933);
#14768=AXIS2_PLACEMENT_3D('',#20745,#16934,#16935);
#14769=AXIS2_PLACEMENT_3D('',#20747,#16937,#16938);
#14770=AXIS2_PLACEMENT_3D('',#20748,#16939,#16940);
#14771=AXIS2_PLACEMENT_3D('',#20757,#16945,#16946);
#14772=AXIS2_PLACEMENT_3D('',#20763,#16950,#16951);
#14773=AXIS2_PLACEMENT_3D('',#20769,#16955,#16956);
#14774=AXIS2_PLACEMENT_3D('',#20775,#16960,#16961);
#14775=AXIS2_PLACEMENT_3D('',#20781,#16965,#16966);
#14776=AXIS2_PLACEMENT_3D('',#20784,#16969,#16970);
#14777=AXIS2_PLACEMENT_3D('',#20785,#16971,#16972);
#16897=DIRECTION('axis',(0.,0.,1.));
#16898=DIRECTION('refdir',(1.,0.,0.));
#16899=DIRECTION('center_axis',(0.,1.,0.));
#16900=DIRECTION('ref_axis',(0.,0.,1.));
#16901=DIRECTION('center_axis',(0.,-1.,0.));
#16902=DIRECTION('ref_axis',(1.,0.,0.));
#16903=DIRECTION('center_axis',(0.,-1.,0.));
#16904=DIRECTION('ref_axis',(1.,0.,0.));
#16905=DIRECTION('center_axis',(0.,-1.,0.));
#16906=DIRECTION('ref_axis',(1.,0.,0.));
#16907=DIRECTION('',(0.707106781186548,0.707106781186547,8.65956056235493E-17));
#16908=DIRECTION('center_axis',(0.,-1.,0.));
#16909=DIRECTION('ref_axis',(1.,0.,0.));
#16910=DIRECTION('center_axis',(0.,-1.,0.));
#16911=DIRECTION('ref_axis',(1.,0.,0.));
#16912=DIRECTION('',(0.,1.,0.));
#16913=DIRECTION('center_axis',(0.,1.,0.));
#16914=DIRECTION('ref_axis',(1.,0.,0.));
#16915=DIRECTION('center_axis',(0.,-1.,0.));
#16916=DIRECTION('ref_axis',(1.,0.,0.));
#16917=DIRECTION('',(-0.707106781186547,0.707106781186548,-8.65956056235493E-17));
#16918=DIRECTION('center_axis',(0.,-1.,0.));
#16919=DIRECTION('ref_axis',(0.,0.,-1.));
#16920=DIRECTION('center_axis',(0.,-1.,0.));
#16921=DIRECTION('ref_axis',(1.,0.,0.));
#16922=DIRECTION('center_axis',(0.,1.,0.));
#16923=DIRECTION('ref_axis',(1.,0.,0.));
#16924=DIRECTION('center_axis',(0.,1.,0.));
#16925=DIRECTION('ref_axis',(1.,0.,0.));
#16926=DIRECTION('',(-0.447213595499958,0.894427190999916,-5.47678698264203E-17));
#16927=DIRECTION('center_axis',(0.,-1.,0.));
#16928=DIRECTION('ref_axis',(1.,0.,0.));
#16929=DIRECTION('center_axis',(0.,1.,0.));
#16930=DIRECTION('ref_axis',(1.,0.,0.));
#16931=DIRECTION('',(0.,1.,0.));
#16932=DIRECTION('center_axis',(0.,1.,0.));
#16933=DIRECTION('ref_axis',(1.,0.,0.));
#16934=DIRECTION('center_axis',(0.,-1.,0.));
#16935=DIRECTION('ref_axis',(1.,0.,0.));
#16936=DIRECTION('',(-0.707106781186547,0.707106781186548,-8.65956056235493E-17));
#16937=DIRECTION('center_axis',(0.,-1.,0.));
#16938=DIRECTION('ref_axis',(0.,0.,-1.));
#16939=DIRECTION('center_axis',(0.866025403784439,0.,-0.5));
#16940=DIRECTION('ref_axis',(0.5,0.,0.866025403784439));
#16941=DIRECTION('',(-0.5,0.,-0.866025403784439));
#16942=DIRECTION('',(0.,-1.,0.));
#16943=DIRECTION('',(0.5,0.,0.866025403784439));
#16944=DIRECTION('',(0.,-1.,0.));
#16945=DIRECTION('center_axis',(1.20185167898973E-16,0.,-1.));
#16946=DIRECTION('ref_axis',(1.,0.,1.20185167898973E-16));
#16947=DIRECTION('',(-1.,0.,-1.20185167898973E-16));
#16948=DIRECTION('',(0.,-1.,0.));
#16949=DIRECTION('',(1.,0.,1.20185167898973E-16));
#16950=DIRECTION('center_axis',(-0.866025403784439,0.,-0.5));
#16951=DIRECTION('ref_axis',(0.5,0.,-0.866025403784439));
#16952=DIRECTION('',(-0.5,0.,0.866025403784439));
#16953=DIRECTION('',(0.,-1.,0.));
#16954=DIRECTION('',(0.5,0.,-0.866025403784439));
#16955=DIRECTION('center_axis',(-0.866025403784439,0.,0.5));
#16956=DIRECTION('ref_axis',(-0.5,0.,-0.866025403784439));
#16957=DIRECTION('',(0.5,0.,0.866025403784439));
#16958=DIRECTION('',(0.,-1.,0.));
#16959=DIRECTION('',(-0.5,0.,-0.866025403784439));
#16960=DIRECTION('center_axis',(-2.40370335797945E-16,0.,1.));
#16961=DIRECTION('ref_axis',(-1.,0.,-2.40370335797945E-16));
#16962=DIRECTION('',(1.,0.,2.40370335797945E-16));
#16963=DIRECTION('',(0.,-1.,0.));
#16964=DIRECTION('',(-1.,0.,-2.40370335797945E-16));
#16965=DIRECTION('center_axis',(0.866025403784439,0.,0.5));
#16966=DIRECTION('ref_axis',(-0.5,0.,0.866025403784439));
#16967=DIRECTION('',(0.5,0.,-0.866025403784439));
#16968=DIRECTION('',(-0.5,0.,0.866025403784439));
#16969=DIRECTION('center_axis',(0.,1.,0.));
#16970=DIRECTION('ref_axis',(1.,0.,0.));
#16971=DIRECTION('center_axis',(0.,-1.,0.));
#16972=DIRECTION('ref_axis',(0.,0.,-1.));
#20716=CARTESIAN_POINT('',(0.,0.,0.));
#20717=CARTESIAN_POINT('Origin',(0.375,0.5,0.));
#20718=CARTESIAN_POINT('',(-0.375,0.5,-4.59242549680257E-17));
#20719=CARTESIAN_POINT('Origin',(0.,0.5,0.));
#20720=CARTESIAN_POINT('Origin',(0.,0.475,0.));
#20721=CARTESIAN_POINT('',(-0.425,0.45,-5.20474889637625E-17));
#20722=CARTESIAN_POINT('Origin',(0.,0.45,0.));
#20723=CARTESIAN_POINT('',(-0.4,0.475,-4.89858719658941E-17));
#20724=CARTESIAN_POINT('Origin',(0.,0.24,0.));
#20725=CARTESIAN_POINT('',(-0.425,0.0299999999999998,-5.20474889637625E-17));
#20726=CARTESIAN_POINT('Origin',(0.,0.0299999999999998,0.));
#20727=CARTESIAN_POINT('',(-0.425,0.24,-5.20474889637625E-17));
#20728=CARTESIAN_POINT('Origin',(0.,0.0150000000000001,0.));
#20729=CARTESIAN_POINT('',(-0.395,4.85722573273506E-17,-4.83735485663204E-17));
#20730=CARTESIAN_POINT('Origin',(0.,0.,0.));
#20731=CARTESIAN_POINT('',(-0.41,0.0150000000000001,-5.02105187650415E-17));
#20732=CARTESIAN_POINT('Origin',(0.27,0.,0.));
#20733=CARTESIAN_POINT('',(-0.27,0.,-3.30654635769785E-17));
#20734=CARTESIAN_POINT('Origin',(0.,0.,0.));
#20735=CARTESIAN_POINT('Origin',(0.,-0.02,0.));
#20736=CARTESIAN_POINT('',(-0.24505,-0.0498999999999999,3.00099698131059E-17));
#20737=CARTESIAN_POINT('Origin',(0.,-0.0498999999999999,0.));
#20738=CARTESIAN_POINT('',(-0.26,-0.02,-3.18408167778312E-17));
#20739=CARTESIAN_POINT('Origin',(0.,-0.995,0.));
#20740=CARTESIAN_POINT('',(-0.24505,-1.95495,3.00099698131059E-17));
#20741=CARTESIAN_POINT('Origin',(0.,-1.95495,0.));
#20742=CARTESIAN_POINT('',(-0.24505,-0.995,-3.00099698131059E-17));
#20743=CARTESIAN_POINT('Origin',(0.,-1.975,0.));
#20744=CARTESIAN_POINT('',(-0.2,-2.,-2.44929359829471E-17));
#20745=CARTESIAN_POINT('Origin',(0.,-2.,0.));
#20746=CARTESIAN_POINT('',(-0.225,-1.975,-2.75545529808154E-17));
#20747=CARTESIAN_POINT('Origin',(0.,-2.,0.));
#20748=CARTESIAN_POINT('Origin',(0.115470053837925,-0.5,-0.2));
#20749=CARTESIAN_POINT('',(0.23094010767585,-0.5,0.));
#20750=CARTESIAN_POINT('',(0.115470053837925,-0.5,-0.2));
#20751=CARTESIAN_POINT('',(0.23094010767585,-0.5,0.));
#20752=CARTESIAN_POINT('',(0.115470053837925,-0.8,-0.2));
#20753=CARTESIAN_POINT('',(0.115470053837925,-0.5,-0.2));
#20754=CARTESIAN_POINT('',(0.23094010767585,-0.8,0.));
#20755=CARTESIAN_POINT('',(0.23094010767585,-0.8,0.));
#20756=CARTESIAN_POINT('',(0.23094010767585,-0.5,0.));
#20757=CARTESIAN_POINT('Origin',(-0.115470053837925,-0.5,-0.2));
#20758=CARTESIAN_POINT('',(-0.115470053837925,-0.5,-0.2));
#20759=CARTESIAN_POINT('',(0.115470053837925,-0.5,-0.2));
#20760=CARTESIAN_POINT('',(-0.115470053837925,-0.8,-0.2));
#20761=CARTESIAN_POINT('',(-0.115470053837925,-0.5,-0.2));
#20762=CARTESIAN_POINT('',(0.115470053837925,-0.8,-0.2));
#20763=CARTESIAN_POINT('Origin',(-0.23094010767585,-0.5,-2.77555756156289E-17));
#20764=CARTESIAN_POINT('',(-0.23094010767585,-0.5,-2.82820063659975E-17));
#20765=CARTESIAN_POINT('',(-0.115470053837925,-0.5,-0.2));
#20766=CARTESIAN_POINT('',(-0.23094010767585,-0.8,-2.77555756156289E-17));
#20767=CARTESIAN_POINT('',(-0.23094010767585,-0.5,-2.82820063659975E-17));
#20768=CARTESIAN_POINT('',(-0.115470053837925,-0.8,-0.2));
#20769=CARTESIAN_POINT('Origin',(-0.115470053837925,-0.5,0.2));
#20770=CARTESIAN_POINT('',(-0.115470053837925,-0.5,0.2));
#20771=CARTESIAN_POINT('',(-0.23094010767585,-0.5,-2.82820063659975E-17));
#20772=CARTESIAN_POINT('',(-0.115470053837925,-0.8,0.2));
#20773=CARTESIAN_POINT('',(-0.115470053837925,-0.5,0.2));
#20774=CARTESIAN_POINT('',(-0.23094010767585,-0.8,-2.82820063659975E-17));
#20775=CARTESIAN_POINT('Origin',(0.115470053837925,-0.5,0.2));
#20776=CARTESIAN_POINT('',(0.115470053837925,-0.5,0.2));
#20777=CARTESIAN_POINT('',(-0.115470053837925,-0.5,0.2));
#20778=CARTESIAN_POINT('',(0.115470053837925,-0.8,0.2));
#20779=CARTESIAN_POINT('',(0.115470053837925,-0.5,0.2));
#20780=CARTESIAN_POINT('',(-0.115470053837925,-0.8,0.2));
#20781=CARTESIAN_POINT('Origin',(0.23094010767585,-0.5,0.));
#20782=CARTESIAN_POINT('',(0.115470053837925,-0.5,0.2));
#20783=CARTESIAN_POINT('',(0.115470053837925,-0.8,0.2));
#20784=CARTESIAN_POINT('Origin',(0.,-0.5,0.));
#20785=CARTESIAN_POINT('Origin',(0.,-0.8,0.));
#34764=UNCERTAINTY_MEASURE_WITH_UNIT(LENGTH_MEASURE(0.001),#34852,
'DISTANCE_ACCURACY_VALUE',
'Maximum model space distance between geometric entities at asserted c
onnectivities');
#34797=UNCERTAINTY_MEASURE_WITH_UNIT(LENGTH_MEASURE(0.001),#34852,
'DISTANCE_ACCURACY_VALUE',
'Maximum model space distance between geometric entities at asserted c
onnectivities');
#34818=(
GEOMETRIC_REPRESENTATION_CONTEXT(3)
GLOBAL_UNCERTAINTY_ASSIGNED_CONTEXT((#34764))
GLOBAL_UNIT_ASSIGNED_CONTEXT((#34852,#34854,#34855))
REPRESENTATION_CONTEXT('','3D')
);
#34851=(
GEOMETRIC_REPRESENTATION_CONTEXT(3)
GLOBAL_UNCERTAINTY_ASSIGNED_CONTEXT((#34797))
GLOBAL_UNIT_ASSIGNED_CONTEXT((#34852,#34854,#34855))
REPRESENTATION_CONTEXT('','3D')
);
#34852=(
LENGTH_UNIT()
NAMED_UNIT(*)
SI_UNIT(.CENTI.,.METRE.)
);
#34854=(
NAMED_UNIT(*)
PLANE_ANGLE_UNIT()
SI_UNIT($,.RADIAN.)
);
#34855=(
NAMED_UNIT(*)
SI_UNIT($,.STERADIAN.)
SOLID_ANGLE_UNIT()
);
#34876=SHAPE_DEFINITION_REPRESENTATION(#34929,#35093);
#34929=PRODUCT_DEFINITION_SHAPE('',$,#35147);
#35093=SHAPE_REPRESENTATION('',(#14752),#34818);
#35126=PRODUCT_DEFINITION_CONTEXT('part definition',#35287,'design');
#35147=PRODUCT_DEFINITION('Cap Screw - M5x20','Cap Screw - M5x20',#35200,
#35126);
#35200=PRODUCT_DEFINITION_FORMATION('',$,#35309);
#35287=APPLICATION_CONTEXT(
'Core Data for Automotive Mechanical Design Process');
#35288=PRODUCT_CONTEXT('part definition',#35287,'mechanical');
#35309=PRODUCT('Cap Screw - M5x20','Cap Screw - M5x20',
'Cap Screw - M5x20',(#35288));
#35412=COLOUR_RGB('Black',0.12,0.14,0.17);
#35413=FILL_AREA_STYLE_COLOUR('',#35412);
#35414=FILL_AREA_STYLE('',(#35413));
#35415=SURFACE_STYLE_FILL_AREA(#35414);
#35416=SURFACE_SIDE_STYLE('',(#35415));
#35417=SURFACE_STYLE_USAGE(.BOTH.,#35416);
#35418=PRESENTATION_STYLE_ASSIGNMENT((#35417));
ENDSEC;
END-ISO-10303-21;
